ISO-10303-21;
HEADER;
/* Generated by software containing ST-Developer
 * from STEP Tools, Inc. (www.steptools.com) 
 */
/* OPTION: using custom renumber hook */

FILE_DESCRIPTION(
/* description */ ('STEP AP242 Edition 2', 'CAx-IF Rec.Pracs.---Representation and Presentation of Product Manufa
cturing Information (PMI)---4.0---2014-10-13', 'CAx-IF Rec.Pracs.---3D Tessellated Geometry---0.4---2014-09-14', '2;1', 'CAx-IF Rec.Pracs.---User Defined Attributes---1.5---2016-08-15'),
/* implementation_level */ '2;1');

FILE_NAME(
/* name */ 'angular contact ball bearing_68_bsi_BS 6267 ABB - 4815 - 18,SI,NC,18__68__ DE    23193.step',
/* time_stamp */ '2026-10-09T00:23:50Z',
/* author */ (''),
/* organization */ (''),
/* preprocessor_version */ 'ST-DEVELOPER v20',
/* originating_system */ 'ONSHAPE BY PTC INC, 1.221',
/* authorisation */ '  ');

FILE_SCHEMA (('AP242_MANAGED_MODEL_BASED_3D_ENGINEERING_MIM_LF { 1 0 10303 442 3 1 4 }'));
ENDSEC;

DATA;
#54=TOROIDAL_SURFACE('',#8614,0.0117000000001705,0.000300000000224998);
#55=TOROIDAL_SURFACE('',#8623,0.0117000000001705,0.000300000000224998);
#56=TOROIDAL_SURFACE('',#8625,0.00974999999980933,0.00134999999974855);
#57=TOROIDAL_SURFACE('',#8626,0.00974999999980933,0.00134999999974855);
#58=TOROIDAL_SURFACE('',#8637,0.00975000000019067,0.00134999999974855);
#59=TOROIDAL_SURFACE('',#8638,0.00975000000019067,0.00134999999974855);
#60=TOROIDAL_SURFACE('',#8640,0.00779999999982954,0.000300000000224997);
#61=TOROIDAL_SURFACE('',#8641,0.00779999999982954,0.000300000000224997);
#62=TOROIDAL_SURFACE('',#8650,0.00779999999982955,0.000300000000225003);
#63=TOROIDAL_SURFACE('',#8651,0.00779999999982955,0.000300000000225003);
#146=SHAPE_REPRESENTATION_RELATIONSHIP('','',#8236,#152);
#152=ADVANCED_BREP_SHAPE_REPRESENTATION('',(#8222),#18814);
#507=B_SPLINE_CURVE_WITH_KNOTS('',3,(#13340,#13341,#13342,#13343,#13344,
#13345,#13346,#13347,#13348,#13349,#13350),.UNSPECIFIED.,.F.,.F.,(4,1,1,
1,1,1,1,1,4),(6.5285800070357E-11,0.125000000047178,0.25000000002907,0.375000000010962,
0.499999999992854,0.624999999974746,0.749999999956638,0.87499999993853,
0.999999999920422),.UNSPECIFIED.);
#508=B_SPLINE_CURVE_WITH_KNOTS('',3,(#13360,#13361,#13362,#13363,#13364,
#13365,#13366,#13367,#13368,#13369,#13370),.UNSPECIFIED.,.F.,.F.,(4,1,1,
1,1,1,1,1,4),(0.,0.125,0.25,0.375,0.5,0.625,0.75,0.875,1.),
 .UNSPECIFIED.);
#509=B_SPLINE_CURVE_WITH_KNOTS('',3,(#13375,#13376,#13377,#13378,#13379,
#13380,#13381,#13382,#13383,#13384,#13385),.UNSPECIFIED.,.F.,.F.,(4,1,1,
1,1,1,1,1,4),(0.,0.125,0.25,0.375,0.5,0.625,0.75,0.875,1.),
 .UNSPECIFIED.);
#510=B_SPLINE_CURVE_WITH_KNOTS('',3,(#13393,#13394,#13395,#13396,#13397),
 .UNSPECIFIED.,.F.,.F.,(4,1,4),(0.,0.499999978485393,0.999999956970785),
 .UNSPECIFIED.);
#511=B_SPLINE_CURVE_WITH_KNOTS('',3,(#13399,#13400,#13401,#13402,#13403,
#13404,#13405,#13406,#13407,#13408,#13409),.UNSPECIFIED.,.F.,.F.,(4,1,1,
1,1,1,1,1,4),(1.08159811971616E-10,0.125000000086479,0.250000000064798,
0.375000000043118,0.500000000021437,0.624999999999756,0.749999999978076,
0.874999999956395,0.999999999934714),.UNSPECIFIED.);
#512=B_SPLINE_CURVE_WITH_KNOTS('',3,(#13411,#13412,#13413,#13414,#13415),
 .UNSPECIFIED.,.F.,.F.,(4,1,4),(4.3029215375297E-8,0.49999997764101,0.999999912252804),
 .UNSPECIFIED.);
#513=B_SPLINE_CURVE_WITH_KNOTS('',3,(#13425,#13426,#13427,#13428,#13429,
#13430,#13431,#13432,#13433,#13434,#13435),.UNSPECIFIED.,.F.,.F.,(4,1,1,
1,1,1,1,1,4),(0.,0.125,0.25,0.375,0.5,0.625,0.75,0.875,1.),
 .UNSPECIFIED.);
#514=B_SPLINE_CURVE_WITH_KNOTS('',3,(#13445,#13446,#13447,#13448,#13449),
 .UNSPECIFIED.,.F.,.F.,(4,1,4),(2.91751359515211E-8,0.499999949957411,0.999999870739685),
 .UNSPECIFIED.);
#515=B_SPLINE_CURVE_WITH_KNOTS('',3,(#13451,#13452,#13453,#13454,#13455),
 .UNSPECIFIED.,.F.,.F.,(4,1,4),(0.,0.499999985412432,0.999999970824864),
 .UNSPECIFIED.);
#516=B_SPLINE_CURVE_WITH_KNOTS('',3,(#13457,#13458,#13459,#13460,#13461,
#13462,#13463,#13464,#13465,#13466,#13467),.UNSPECIFIED.,.F.,.F.,(4,1,1,
1,1,1,1,1,4),(2.37190894409548E-10,0.125000000203969,0.250000000170748,
0.375000000137526,0.500000000104304,0.625000000071083,0.750000000037861,
0.875000000004639,0.999999999971418),.UNSPECIFIED.);
#517=B_SPLINE_CURVE_WITH_KNOTS('',3,(#13471,#13472,#13473,#13474),
 .UNSPECIFIED.,.F.,.F.,(4,4),(0.,1.),.UNSPECIFIED.);
#518=B_SPLINE_CURVE_WITH_KNOTS('',3,(#13476,#13477,#13478,#13479),
 .UNSPECIFIED.,.F.,.F.,(4,4),(0.,1.),.UNSPECIFIED.);
#519=B_SPLINE_CURVE_WITH_KNOTS('',3,(#13481,#13482,#13483,#13484,#13485,
#13486,#13487),.UNSPECIFIED.,.F.,.F.,(4,1,1,1,4),(1.82135136395292E-10,
0.25000000012028,0.500000000058424,0.749999999996569,0.999999999934713),
 .UNSPECIFIED.);
#520=B_SPLINE_CURVE_WITH_KNOTS('',3,(#13494,#13495,#13496,#13497,#13498,
#13499,#13500),.UNSPECIFIED.,.F.,.F.,(4,1,1,1,4),(0.,0.25,0.5,0.75,1.),
 .UNSPECIFIED.);
#521=B_SPLINE_CURVE_WITH_KNOTS('',3,(#13510,#13511,#13512,#13513),
 .UNSPECIFIED.,.F.,.F.,(4,4),(0.,1.),.UNSPECIFIED.);
#522=B_SPLINE_CURVE_WITH_KNOTS('',3,(#13514,#13515,#13516,#13517),
 .UNSPECIFIED.,.F.,.F.,(4,4),(0.,1.),.UNSPECIFIED.);
#1039=PLANE('',#8617);
#1040=PLANE('',#8628);
#1041=PLANE('',#8634);
#1042=PLANE('',#8647);
#2122=ORIENTED_EDGE('',*,*,#3982,.T.);
#2123=ORIENTED_EDGE('',*,*,#3983,.T.);
#2124=ORIENTED_EDGE('',*,*,#3984,.T.);
#2125=ORIENTED_EDGE('',*,*,#3984,.F.);
#2126=ORIENTED_EDGE('',*,*,#3985,.T.);
#2127=ORIENTED_EDGE('',*,*,#3986,.T.);
#2128=ORIENTED_EDGE('',*,*,#3987,.T.);
#2129=ORIENTED_EDGE('',*,*,#3983,.F.);
#2130=ORIENTED_EDGE('',*,*,#3982,.F.);
#2131=ORIENTED_EDGE('',*,*,#3985,.F.);
#2132=ORIENTED_EDGE('',*,*,#3988,.F.);
#2133=ORIENTED_EDGE('',*,*,#3989,.F.);
#2134=ORIENTED_EDGE('',*,*,#3990,.T.);
#2135=ORIENTED_EDGE('',*,*,#3987,.F.);
#2136=ORIENTED_EDGE('',*,*,#3986,.F.);
#2137=ORIENTED_EDGE('',*,*,#3991,.T.);
#2138=ORIENTED_EDGE('',*,*,#3992,.T.);
#2139=ORIENTED_EDGE('',*,*,#3993,.T.);
#2140=ORIENTED_EDGE('',*,*,#3988,.T.);
#2141=ORIENTED_EDGE('',*,*,#3994,.T.);
#2142=ORIENTED_EDGE('',*,*,#3991,.F.);
#2143=ORIENTED_EDGE('',*,*,#3989,.T.);
#2144=ORIENTED_EDGE('',*,*,#3993,.F.);
#2145=ORIENTED_EDGE('',*,*,#3990,.F.);
#2146=ORIENTED_EDGE('',*,*,#3995,.T.);
#2147=ORIENTED_EDGE('',*,*,#3994,.F.);
#2148=ORIENTED_EDGE('',*,*,#3992,.F.);
#2149=ORIENTED_EDGE('',*,*,#3996,.T.);
#2150=ORIENTED_EDGE('',*,*,#3997,.F.);
#2151=ORIENTED_EDGE('',*,*,#3998,.F.);
#2152=ORIENTED_EDGE('',*,*,#3995,.F.);
#2153=ORIENTED_EDGE('',*,*,#3996,.F.);
#2154=ORIENTED_EDGE('',*,*,#3999,.T.);
#2155=ORIENTED_EDGE('',*,*,#4000,.T.);
#2156=ORIENTED_EDGE('',*,*,#4001,.T.);
#2157=ORIENTED_EDGE('',*,*,#3997,.T.);
#2158=ORIENTED_EDGE('',*,*,#4002,.T.);
#2159=ORIENTED_EDGE('',*,*,#4003,.T.);
#2160=ORIENTED_EDGE('',*,*,#3998,.T.);
#2161=ORIENTED_EDGE('',*,*,#4001,.F.);
#2162=ORIENTED_EDGE('',*,*,#4004,.T.);
#2163=ORIENTED_EDGE('',*,*,#4002,.F.);
#2164=ORIENTED_EDGE('',*,*,#4005,.T.);
#2165=ORIENTED_EDGE('',*,*,#4000,.F.);
#2166=ORIENTED_EDGE('',*,*,#4006,.T.);
#2167=ORIENTED_EDGE('',*,*,#4007,.T.);
#2168=ORIENTED_EDGE('',*,*,#3999,.F.);
#2169=ORIENTED_EDGE('',*,*,#4005,.F.);
#2170=ORIENTED_EDGE('',*,*,#4008,.T.);
#2171=ORIENTED_EDGE('',*,*,#4006,.F.);
#2172=ORIENTED_EDGE('',*,*,#4009,.T.);
#2173=ORIENTED_EDGE('',*,*,#4003,.F.);
#2174=ORIENTED_EDGE('',*,*,#4004,.F.);
#2175=ORIENTED_EDGE('',*,*,#4007,.F.);
#2176=ORIENTED_EDGE('',*,*,#4008,.F.);
#2177=ORIENTED_EDGE('',*,*,#4010,.F.);
#2178=ORIENTED_EDGE('',*,*,#4011,.F.);
#2179=ORIENTED_EDGE('',*,*,#4009,.F.);
#2180=ORIENTED_EDGE('',*,*,#4012,.T.);
#2181=ORIENTED_EDGE('',*,*,#4013,.T.);
#2182=ORIENTED_EDGE('',*,*,#4014,.T.);
#2183=ORIENTED_EDGE('',*,*,#4010,.T.);
#2184=ORIENTED_EDGE('',*,*,#4015,.T.);
#2185=ORIENTED_EDGE('',*,*,#4013,.F.);
#2186=ORIENTED_EDGE('',*,*,#4011,.T.);
#2187=ORIENTED_EDGE('',*,*,#4014,.F.);
#2188=ORIENTED_EDGE('',*,*,#4012,.F.);
#2189=ORIENTED_EDGE('',*,*,#4015,.F.);
#3982=EDGE_CURVE('',#4997,#4998,#507,.T.);
#3983=EDGE_CURVE('',#4998,#4997,#5661,.T.);
#3984=EDGE_CURVE('',#4999,#4999,#5662,.F.);
#3985=EDGE_CURVE('',#5000,#5000,#5663,.F.);
#3986=EDGE_CURVE('',#5001,#5002,#508,.F.);
#3987=EDGE_CURVE('',#5002,#5001,#5664,.T.);
#3988=EDGE_CURVE('',#5003,#5004,#509,.F.);
#3989=EDGE_CURVE('',#5004,#5003,#5665,.T.);
#3990=EDGE_CURVE('',#5005,#5005,#5666,.T.);
#3991=EDGE_CURVE('',#5004,#5006,#510,.T.);
#3992=EDGE_CURVE('',#5006,#5007,#511,.T.);
#3993=EDGE_CURVE('',#5007,#5003,#512,.T.);
#3994=EDGE_CURVE('',#5007,#5006,#5667,.F.);
#3995=EDGE_CURVE('',#5008,#5008,#5668,.T.);
#3996=EDGE_CURVE('',#5009,#5009,#5669,.F.);
#3997=EDGE_CURVE('',#5010,#5011,#513,.F.);
#3998=EDGE_CURVE('',#5011,#5010,#5670,.F.);
#3999=EDGE_CURVE('',#5012,#5013,#5671,.F.);
#4000=EDGE_CURVE('',#5013,#5012,#5672,.F.);
#4001=EDGE_CURVE('',#5014,#5010,#514,.T.);
#4002=EDGE_CURVE('',#5011,#5015,#515,.T.);
#4003=EDGE_CURVE('',#5015,#5014,#516,.T.);
#4004=EDGE_CURVE('',#5014,#5015,#5673,.T.);
#4005=EDGE_CURVE('',#5016,#5012,#517,.T.);
#4006=EDGE_CURVE('',#5013,#5017,#518,.T.);
#4007=EDGE_CURVE('',#5017,#5016,#519,.T.);
#4008=EDGE_CURVE('',#5016,#5017,#5674,.F.);
#4009=EDGE_CURVE('',#5018,#5018,#5675,.T.);
#4010=EDGE_CURVE('',#5019,#5020,#520,.F.);
#4011=EDGE_CURVE('',#5020,#5019,#5676,.T.);
#4012=EDGE_CURVE('',#5021,#5022,#5677,.T.);
#4013=EDGE_CURVE('',#5022,#5021,#5678,.T.);
#4014=EDGE_CURVE('',#5022,#5019,#521,.T.);
#4015=EDGE_CURVE('',#5020,#5021,#522,.T.);
#4997=VERTEX_POINT('',#13351);
#4998=VERTEX_POINT('',#13352);
#4999=VERTEX_POINT('',#13355);
#5000=VERTEX_POINT('',#13358);
#5001=VERTEX_POINT('',#13371);
#5002=VERTEX_POINT('',#13372);
#5003=VERTEX_POINT('',#13386);
#5004=VERTEX_POINT('',#13387);
#5005=VERTEX_POINT('',#13391);
#5006=VERTEX_POINT('',#13398);
#5007=VERTEX_POINT('',#13410);
#5008=VERTEX_POINT('',#13420);
#5009=VERTEX_POINT('',#13423);
#5010=VERTEX_POINT('',#13436);
#5011=VERTEX_POINT('',#13437);
#5012=VERTEX_POINT('',#13441);
#5013=VERTEX_POINT('',#13442);
#5014=VERTEX_POINT('',#13450);
#5015=VERTEX_POINT('',#13456);
#5016=VERTEX_POINT('',#13475);
#5017=VERTEX_POINT('',#13480);
#5018=VERTEX_POINT('',#13492);
#5019=VERTEX_POINT('',#13501);
#5020=VERTEX_POINT('',#13502);
#5021=VERTEX_POINT('',#13506);
#5022=VERTEX_POINT('',#13507);
#5661=CIRCLE('',#8615,0.0120000000003955);
#5662=CIRCLE('',#8616,0.0117000000001921);
#5663=CIRCLE('',#8618,0.01065);
#5664=CIRCLE('',#8620,0.012);
#5665=CIRCLE('',#8622,0.0106499999992724);
#5666=CIRCLE('',#8624,0.0117000000001921);
#5667=CIRCLE('',#8627,0.00842500000016944);
#5668=CIRCLE('',#8629,0.011075);
#5669=CIRCLE('',#8631,0.008425);
#5670=CIRCLE('',#8633,0.0110749999998306);
#5671=CIRCLE('',#8635,0.00779999999980785);
#5672=CIRCLE('',#8636,0.00779999999980785);
#5673=CIRCLE('',#8639,0.00885000000072759);
#5674=CIRCLE('',#8642,0.00749999999960454);
#5675=CIRCLE('',#8644,0.00885);
#5676=CIRCLE('',#8646,0.00749999999960454);
#5677=CIRCLE('',#8648,0.00779999999980785);
#5678=CIRCLE('',#8649,0.00779999999980785);
#6199=EDGE_LOOP('',(#2122,#2123));
#6200=EDGE_LOOP('',(#2124));
#6201=EDGE_LOOP('',(#2125));
#6202=EDGE_LOOP('',(#2126));
#6203=EDGE_LOOP('',(#2127,#2128));
#6204=EDGE_LOOP('',(#2129,#2130));
#6205=EDGE_LOOP('',(#2131));
#6206=EDGE_LOOP('',(#2132,#2133));
#6207=EDGE_LOOP('',(#2134));
#6208=EDGE_LOOP('',(#2135,#2136));
#6209=EDGE_LOOP('',(#2137,#2138,#2139,#2140));
#6210=EDGE_LOOP('',(#2141,#2142,#2143,#2144));
#6211=EDGE_LOOP('',(#2145));
#6212=EDGE_LOOP('',(#2146));
#6213=EDGE_LOOP('',(#2147,#2148));
#6214=EDGE_LOOP('',(#2149));
#6215=EDGE_LOOP('',(#2150,#2151));
#6216=EDGE_LOOP('',(#2152));
#6217=EDGE_LOOP('',(#2153));
#6218=EDGE_LOOP('',(#2154,#2155));
#6219=EDGE_LOOP('',(#2156,#2157,#2158,#2159));
#6220=EDGE_LOOP('',(#2160,#2161,#2162,#2163));
#6221=EDGE_LOOP('',(#2164,#2165,#2166,#2167));
#6222=EDGE_LOOP('',(#2168,#2169,#2170,#2171));
#6223=EDGE_LOOP('',(#2172));
#6224=EDGE_LOOP('',(#2173,#2174));
#6225=EDGE_LOOP('',(#2175,#2176));
#6226=EDGE_LOOP('',(#2177,#2178));
#6227=EDGE_LOOP('',(#2179));
#6228=EDGE_LOOP('',(#2180,#2181));
#6229=EDGE_LOOP('',(#2182,#2183,#2184,#2185));
#6230=EDGE_LOOP('',(#2186,#2187,#2188,#2189));
#6960=FACE_BOUND('',#6199,.T.);
#6961=FACE_BOUND('',#6200,.T.);
#6962=FACE_BOUND('',#6201,.T.);
#6963=FACE_BOUND('',#6202,.T.);
#6964=FACE_BOUND('',#6203,.T.);
#6965=FACE_BOUND('',#6204,.T.);
#6966=FACE_BOUND('',#6205,.T.);
#6967=FACE_BOUND('',#6206,.T.);
#6968=FACE_BOUND('',#6207,.T.);
#6969=FACE_BOUND('',#6208,.T.);
#6970=FACE_BOUND('',#6209,.T.);
#6971=FACE_BOUND('',#6210,.T.);
#6972=FACE_BOUND('',#6211,.T.);
#6973=FACE_BOUND('',#6212,.T.);
#6974=FACE_BOUND('',#6213,.T.);
#6975=FACE_BOUND('',#6214,.T.);
#6976=FACE_BOUND('',#6215,.T.);
#6977=FACE_BOUND('',#6216,.T.);
#6978=FACE_BOUND('',#6217,.T.);
#6979=FACE_BOUND('',#6218,.T.);
#6980=FACE_BOUND('',#6219,.T.);
#6981=FACE_BOUND('',#6220,.T.);
#6982=FACE_BOUND('',#6221,.T.);
#6983=FACE_BOUND('',#6222,.T.);
#6984=FACE_BOUND('',#6223,.T.);
#6985=FACE_BOUND('',#6224,.T.);
#6986=FACE_BOUND('',#6225,.T.);
#6987=FACE_BOUND('',#6226,.T.);
#6988=FACE_BOUND('',#6227,.T.);
#6989=FACE_BOUND('',#6228,.T.);
#6990=FACE_BOUND('',#6229,.T.);
#6991=FACE_BOUND('',#6230,.T.);
#7511=CYLINDRICAL_SURFACE('',#8619,0.012);
#7512=CYLINDRICAL_SURFACE('',#8621,0.01065);
#7513=CYLINDRICAL_SURFACE('',#8630,0.008425);
#7514=CYLINDRICAL_SURFACE('',#8632,0.011075);
#7515=CYLINDRICAL_SURFACE('',#8643,0.00885);
#7516=CYLINDRICAL_SURFACE('',#8645,0.0075);
#7873=ADVANCED_FACE('',(#6960,#6961),#54,.T.);
#7874=ADVANCED_FACE('',(#6962,#6963),#1039,.T.);
#7875=ADVANCED_FACE('',(#6964,#6965),#7511,.T.);
#7876=ADVANCED_FACE('',(#6966,#6967),#7512,.F.);
#7877=ADVANCED_FACE('',(#6968,#6969),#55,.T.);
#7878=ADVANCED_FACE('',(#6970),#56,.T.);
#7879=ADVANCED_FACE('',(#6971),#57,.T.);
#7880=ADVANCED_FACE('',(#6972,#6973),#1040,.T.);
#7881=ADVANCED_FACE('',(#6974,#6975),#7513,.T.);
#7882=ADVANCED_FACE('',(#6976,#6977),#7514,.F.);
#7883=ADVANCED_FACE('',(#6978,#6979),#1041,.T.);
#7884=ADVANCED_FACE('',(#6980),#58,.T.);
#7885=ADVANCED_FACE('',(#6981),#59,.T.);
#7886=ADVANCED_FACE('',(#6982),#60,.T.);
#7887=ADVANCED_FACE('',(#6983),#61,.T.);
#7888=ADVANCED_FACE('',(#6984,#6985),#7515,.T.);
#7889=ADVANCED_FACE('',(#6986,#6987),#7516,.F.);
#7890=ADVANCED_FACE('',(#6988,#6989),#1042,.T.);
#7891=ADVANCED_FACE('',(#6990),#62,.T.);
#7892=ADVANCED_FACE('',(#6991),#63,.T.);
#8171=CLOSED_SHELL('',(#7873,#7874,#7875,#7876,#7877,#7878,#7879,#7880,
#7881,#7882,#7883,#7884,#7885,#7886,#7887,#7888,#7889,#7890,#7891,#7892));
#8177=STYLED_ITEM('',(#8183),#8222);
#8183=PRESENTATION_STYLE_ASSIGNMENT((#8189));
#8189=SURFACE_STYLE_USAGE(.BOTH.,#8195);
#8195=SURFACE_SIDE_STYLE('',(#8201));
#8201=SURFACE_STYLE_FILL_AREA(#8207);
#8207=FILL_AREA_STYLE('',(#8213));
#8213=FILL_AREA_STYLE_COLOUR('',#8217);
#8217=COLOUR_RGB('', 0.72549020, 0.75294118, 0.79215686);
#8222=MANIFOLD_SOLID_BREP(
'angular contact ball bearing_68_bsi_BS 6267 ABB - 4815 - 18,SI,NC,18_
68__ DE    23193',#8171);
#8229=SHAPE_DEFINITION_REPRESENTATION(#18834,#8236);
#8236=SHAPE_REPRESENTATION(
'angular contact ball bearing_68_bsi_BS 6267 ABB - 4815 - 18,SI,NC,18_
68__ DE    23193',(#8239),#18814);
#8239=AXIS2_PLACEMENT_3D('',#11098,#9192,#9193);
#8614=AXIS2_PLACEMENT_3D('',#13339,#9942,#9943);
#8615=AXIS2_PLACEMENT_3D('',#13353,#9944,#9945);
#8616=AXIS2_PLACEMENT_3D('',#13354,#9946,#9947);
#8617=AXIS2_PLACEMENT_3D('',#13356,#9948,#9949);
#8618=AXIS2_PLACEMENT_3D('',#13357,#9950,#9951);
#8619=AXIS2_PLACEMENT_3D('',#13359,#9952,#9953);
#8620=AXIS2_PLACEMENT_3D('',#13373,#9954,#9955);
#8621=AXIS2_PLACEMENT_3D('',#13374,#9956,#9957);
#8622=AXIS2_PLACEMENT_3D('',#13388,#9958,#9959);
#8623=AXIS2_PLACEMENT_3D('',#13389,#9960,#9961);
#8624=AXIS2_PLACEMENT_3D('',#13390,#9962,#9963);
#8625=AXIS2_PLACEMENT_3D('',#13392,#9964,#9965);
#8626=AXIS2_PLACEMENT_3D('',#13416,#9966,#9967);
#8627=AXIS2_PLACEMENT_3D('',#13417,#9968,#9969);
#8628=AXIS2_PLACEMENT_3D('',#13418,#9970,#9971);
#8629=AXIS2_PLACEMENT_3D('',#13419,#9972,#9973);
#8630=AXIS2_PLACEMENT_3D('',#13421,#9974,#9975);
#8631=AXIS2_PLACEMENT_3D('',#13422,#9976,#9977);
#8632=AXIS2_PLACEMENT_3D('',#13424,#9978,#9979);
#8633=AXIS2_PLACEMENT_3D('',#13438,#9980,#9981);
#8634=AXIS2_PLACEMENT_3D('',#13439,#9982,#9983);
#8635=AXIS2_PLACEMENT_3D('',#13440,#9984,#9985);
#8636=AXIS2_PLACEMENT_3D('',#13443,#9986,#9987);
#8637=AXIS2_PLACEMENT_3D('',#13444,#9988,#9989);
#8638=AXIS2_PLACEMENT_3D('',#13468,#9990,#9991);
#8639=AXIS2_PLACEMENT_3D('',#13469,#9992,#9993);
#8640=AXIS2_PLACEMENT_3D('',#13470,#9994,#9995);
#8641=AXIS2_PLACEMENT_3D('',#13488,#9996,#9997);
#8642=AXIS2_PLACEMENT_3D('',#13489,#9998,#9999);
#8643=AXIS2_PLACEMENT_3D('',#13490,#10000,#10001);
#8644=AXIS2_PLACEMENT_3D('',#13491,#10002,#10003);
#8645=AXIS2_PLACEMENT_3D('',#13493,#10004,#10005);
#8646=AXIS2_PLACEMENT_3D('',#13503,#10006,#10007);
#8647=AXIS2_PLACEMENT_3D('',#13504,#10008,#10009);
#8648=AXIS2_PLACEMENT_3D('',#13505,#10010,#10011);
#8649=AXIS2_PLACEMENT_3D('',#13508,#10012,#10013);
#8650=AXIS2_PLACEMENT_3D('',#13509,#10014,#10015);
#8651=AXIS2_PLACEMENT_3D('',#13518,#10016,#10017);
#9192=DIRECTION('',(0.,0.,1.));
#9193=DIRECTION('',(1.,0.,0.));
#9942=DIRECTION('',(1.,-4.75612924231451E-12,-4.0043073372981E-18));
#9943=DIRECTION('',(4.75612924231451E-12,1.,0.));
#9944=DIRECTION('',(1.,-4.75612924231451E-12,-4.0043073372981E-18));
#9945=DIRECTION('',(4.75612924231451E-12,1.,0.));
#9946=DIRECTION('',(1.,-4.75612924231451E-12,-4.0043073372981E-18));
#9947=DIRECTION('',(4.75612924231451E-12,1.,0.));
#9948=DIRECTION('',(1.,4.22825609356439E-17,-4.00585564781671E-17));
#9949=DIRECTION('',(-4.22825609356439E-17,1.,0.));
#9950=DIRECTION('',(1.,0.,-1.2509555207044E-16));
#9951=DIRECTION('',(-1.2509555207044E-16,0.,-1.));
#9952=DIRECTION('',(1.,0.,-7.40148683083438E-17));
#9953=DIRECTION('',(-7.40148683083438E-17,0.,-1.));
#9954=DIRECTION('',(1.,0.,-7.40148683083438E-17));
#9955=DIRECTION('',(-7.40148683083438E-17,0.,-1.));
#9956=DIRECTION('',(1.,0.,-1.2509555207044E-16));
#9957=DIRECTION('',(-1.2509555207044E-16,0.,-1.));
#9958=DIRECTION('',(1.,-8.51933299579803E-12,-1.51031137741696E-17));
#9959=DIRECTION('',(8.51933299579803E-12,1.,0.));
#9960=DIRECTION('',(1.,4.75611052379189E-12,2.67348976061206E-17));
#9961=DIRECTION('',(-4.75611052379189E-12,1.,0.));
#9962=DIRECTION('',(1.,4.75611052379189E-12,2.67348976061206E-17));
#9963=DIRECTION('',(-4.75611052379189E-12,1.,0.));
#9964=DIRECTION('',(1.,8.51931011104313E-12,9.10429714682885E-18));
#9965=DIRECTION('',(-8.51931011104313E-12,1.,0.));
#9966=DIRECTION('',(1.,-8.51933299579803E-12,-1.51031137741696E-17));
#9967=DIRECTION('',(8.51933299579803E-12,1.,0.));
#9968=DIRECTION('',(1.,-8.51933299579803E-12,-1.51031137741696E-17));
#9969=DIRECTION('',(8.51933299579803E-12,1.,0.));
#9970=DIRECTION('',(-1.,4.22825609356439E-17,4.00585564781671E-17));
#9971=DIRECTION('',(-4.22825609356439E-17,-1.,0.));
#9972=DIRECTION('',(1.,0.,0.));
#9973=DIRECTION('',(0.,0.,-1.));
#9974=DIRECTION('',(1.,0.,-7.90663281632159E-17));
#9975=DIRECTION('',(-7.90663281632159E-17,0.,-1.));
#9976=DIRECTION('',(1.,0.,-7.90663281632159E-17));
#9977=DIRECTION('',(-7.90663281632159E-17,0.,-1.));
#9978=DIRECTION('',(1.,0.,0.));
#9979=DIRECTION('',(0.,0.,-1.));
#9980=DIRECTION('',(1.,8.51953932343756E-12,7.17449131436051E-18));
#9981=DIRECTION('',(-8.51953932343756E-12,1.,0.));
#9982=DIRECTION('',(1.,5.87188086584048E-17,-5.56302802130048E-17));
#9983=DIRECTION('',(-5.87188086584048E-17,1.,0.));
#9984=DIRECTION('',(1.,-7.13444545520919E-12,-2.65134118218329E-17));
#9985=DIRECTION('',(7.13444545520919E-12,1.,0.));
#9986=DIRECTION('',(1.,7.13442257045429E-12,2.86761022065096E-17));
#9987=DIRECTION('',(-7.13442257045429E-12,1.,0.));
#9988=DIRECTION('',(1.,-8.51956220819246E-12,-1.01389396052301E-18));
#9989=DIRECTION('',(8.51956220819246E-12,1.,0.));
#9990=DIRECTION('',(1.,8.51953932343756E-12,7.17449131436051E-18));
#9991=DIRECTION('',(-8.51953932343756E-12,1.,0.));
#9992=DIRECTION('',(1.,8.51953932343756E-12,7.17449131436051E-18));
#9993=DIRECTION('',(-8.51953932343756E-12,1.,0.));
#9994=DIRECTION('',(1.,7.13442257045429E-12,2.86761022065096E-17));
#9995=DIRECTION('',(-7.13442257045429E-12,1.,0.));
#9996=DIRECTION('',(1.,-7.13444545520919E-12,-2.65134118218329E-17));
#9997=DIRECTION('',(7.13444545520919E-12,1.,0.));
#9998=DIRECTION('',(1.,-7.13444545520919E-12,-2.65134118218329E-17));
#9999=DIRECTION('',(7.13444545520919E-12,1.,0.));
#10000=DIRECTION('',(1.,0.,0.));
#10001=DIRECTION('',(0.,0.,-1.));
#10002=DIRECTION('',(1.,0.,0.));
#10003=DIRECTION('',(0.,0.,-1.));
#10004=DIRECTION('',(1.,0.,-1.1842378929335E-16));
#10005=DIRECTION('',(-1.1842378929335E-16,0.,-1.));
#10006=DIRECTION('',(1.,7.13444719404544E-12,-2.88724849698279E-17));
#10007=DIRECTION('',(-7.13444719404544E-12,1.,0.));
#10008=DIRECTION('',(-1.,5.58989788640793E-17,5.29587695813052E-17));
#10009=DIRECTION('',(-5.58989788640793E-17,-1.,0.));
#10010=DIRECTION('',(1.,7.13444719404544E-12,-2.88724849698279E-17));
#10011=DIRECTION('',(-7.13444719404544E-12,1.,0.));
#10012=DIRECTION('',(1.,-7.13447007880035E-12,4.01455929805839E-17));
#10013=DIRECTION('',(7.13447007880035E-12,1.,0.));
#10014=DIRECTION('',(1.,-7.13447007880035E-12,4.01455929805839E-17));
#10015=DIRECTION('',(7.13447007880035E-12,1.,0.));
#10016=DIRECTION('',(1.,7.13444719404544E-12,-2.88724849698279E-17));
#10017=DIRECTION('',(-7.13444719404544E-12,1.,0.));
#11098=CARTESIAN_POINT('',(0.,0.,0.));
#13339=CARTESIAN_POINT('',(0.00420000000011192,-3.50899506067413E-13,5.47386837469071E-19));
#13340=CARTESIAN_POINT('',(0.00420000000019215,-2.46124009164679E-12,0.0120000000003955));
#13341=CARTESIAN_POINT('',(0.00420000000019962,-0.00157079632905111,0.0120000000000274));
#13342=CARTESIAN_POINT('',(0.00420000000021455,-0.00471165671129617,0.0113751824584622));
#13343=CARTESIAN_POINT('',(0.00420000000023355,-0.00870621415729384,0.00870618773365808));
#13344=CARTESIAN_POINT('',(0.00420000000024625,-0.0113751749099263,0.00471175484862072));
#13345=CARTESIAN_POINT('',(0.00420000000025071,-0.0123124125450508,2.76378563580788E-13));
#13346=CARTESIAN_POINT('',(0.00420000000024625,-0.0113751749101378,-0.00471175484810999));
#13347=CARTESIAN_POINT('',(0.00420000000023355,-0.00870621415768473,-0.00870618773326719));
#13348=CARTESIAN_POINT('',(0.00420000000021456,-0.0047116567118069,-0.0113751824582506));
#13349=CARTESIAN_POINT('',(0.00420000000019962,-0.00157079632958987,-0.0119999999999568));
#13350=CARTESIAN_POINT('',(0.00420000000019215,-3.00000140206592E-12,-0.0120000000003955));
#13351=CARTESIAN_POINT('',(0.00419999987509607,-2.46123887461207E-12,0.0120000000001977));
#13352=CARTESIAN_POINT('',(0.00419999987509607,-3.00000082519295E-12,-0.0120000000001977));
#13353=CARTESIAN_POINT('',(0.00420000000019215,-3.50899506067795E-13,5.47386837468749E-19));
#13354=CARTESIAN_POINT('',(0.00450000000033692,-3.52326344841177E-13,5.4618554526698E-19));
#13355=CARTESIAN_POINT('',(0.00450000000039257,0.0116999999998398,5.4618554526698E-19));
#13356=CARTESIAN_POINT('',(0.0045,-5.3776427755281E-19,-1.47451495458029E-19));
#13357=CARTESIAN_POINT('',(0.0045,0.,-3.14458944017069E-18));
#13358=CARTESIAN_POINT('',(0.0045,0.,-0.01065));
#13359=CARTESIAN_POINT('',(-0.0206375,0.,-4.67643299434448E-52));
#13360=CARTESIAN_POINT('',(-0.0042,-5.15503667236967E-12,-0.012));
#13361=CARTESIAN_POINT('',(-0.0042,-0.00157079633140504,-0.0119999999993252));
#13362=CARTESIAN_POINT('',(-0.0042,-0.00471165671284908,-0.0113751824573995));
#13363=CARTESIAN_POINT('',(-0.0042,-0.0087062141577214,-0.00870618773284344));
#13364=CARTESIAN_POINT('',(-0.0042,-0.0113751749096969,-0.00471175484865801));
#13365=CARTESIAN_POINT('',(-0.0042,-0.0123124125448799,-1.41974949723703E-12));
#13366=CARTESIAN_POINT('',(-0.0042,-0.0113751749107835,0.00471175484603467));
#13367=CARTESIAN_POINT('',(-0.0042,-0.00870621415972922,0.0087061877308356));
#13368=CARTESIAN_POINT('',(-0.0042,-0.00471165671547242,0.0113751824563129));
#13369=CARTESIAN_POINT('',(-0.0042,-0.00157079633417248,0.0119999999989629));
#13370=CARTESIAN_POINT('',(-0.0042,-7.92248253258906E-12,0.012));
#13371=CARTESIAN_POINT('',(-0.00419999987509607,-2.46123798780892E-12,0.0120000000001977));
#13372=CARTESIAN_POINT('',(-0.004199999875,-4.0775188822195E-12,-0.012));
#13373=CARTESIAN_POINT('',(-0.0042,0.,-1.2166193978184E-18));
#13374=CARTESIAN_POINT('',(-0.0206375,0.,0.));
#13375=CARTESIAN_POINT('',(0.00100623059,-4.57509504672808E-12,-0.01065));
#13376=CARTESIAN_POINT('',(0.00100623059,-0.00139408174412197,-0.0106499999994011));
#13377=CARTESIAN_POINT('',(0.00100623059,-0.00418159533265356,-0.0100954744309421));
#13378=CARTESIAN_POINT('',(0.00100623059,-0.00772676506497774,-0.00772674161289855));
#13379=CARTESIAN_POINT('',(0.00100623059,-0.010095467732356,-0.00418168242818399));
#13380=CARTESIAN_POINT('',(0.00100623059,-0.0109272661335809,-1.26002854163711E-12));
#13381=CARTESIAN_POINT('',(0.00100623059,-0.0100954677333204,0.00418168242585576));
#13382=CARTESIAN_POINT('',(0.00100623059,-0.00772676506675968,0.0077267416111166));
#13383=CARTESIAN_POINT('',(0.00100623059,-0.00418159533498178,0.0100954744299777));
#13384=CARTESIAN_POINT('',(0.00100623059,-0.00139408174657808,0.0106499999990796));
#13385=CARTESIAN_POINT('',(0.00100623059,-7.03120324767279E-12,0.01065));
#13386=CARTESIAN_POINT('',(0.00100623096506661,-2.18434900175713E-12,0.0106499999996362));
#13387=CARTESIAN_POINT('',(0.00100623059006661,-4.95004771836549E-12,-0.0106499999996362));
#13388=CARTESIAN_POINT('',(0.00100623059013322,-5.59151227703387E-14,4.31770786296025E-20));
#13389=CARTESIAN_POINT('',(-0.00420000000011192,-3.50900396996374E-13,-2.29851109841953E-19));
#13390=CARTESIAN_POINT('',(-0.00450000000033692,-3.52327230154582E-13,-2.37871579129804E-19));
#13391=CARTESIAN_POINT('',(-0.00450000000039257,0.0116999999998398,-2.37871579129804E-19));
#13392=CARTESIAN_POINT('',(1.154356125671E-13,4.73423576231519E-14,5.99501471359368E-21));
#13393=CARTESIAN_POINT('',(0.00100623059013322,5.05895643960993E-20,-0.0106499999992724));
#13394=CARTESIAN_POINT('',(0.00132239692493253,3.43168701089793E-15,-0.0102965152906072));
#13395=CARTESIAN_POINT('',(0.00153614706478366,8.87052617196055E-15,-0.00923383493259741));
#13396=CARTESIAN_POINT('',(0.000724069227561596,4.32262384432489E-15,-0.00851584589933923));
#13397=CARTESIAN_POINT('',(0.000258602131639666,7.10249954130499E-18,-0.00842500002362359));
#13398=CARTESIAN_POINT('',(0.000258602136233779,-2.86275794301951E-12,-0.00842500000008472));
#13399=CARTESIAN_POINT('',(0.000258602011467558,-2.86275710191455E-12,-0.00842500000016943));
#13400=CARTESIAN_POINT('',(0.000258602011476953,-0.00110282992379344,-0.00842499999978821));
#13401=CARTESIAN_POINT('',(0.00025860201149574,-0.0033079756503873,-0.00798632601725331));
#13402=CARTESIAN_POINT('',(0.000258602011519631,-0.00611248785699539,-0.00611246930397495));
#13403=CARTESIAN_POINT('',(0.000258602011535596,-0.00798632071841419,-0.00330804454916419));
#13404=CARTESIAN_POINT('',(0.000258602011541202,-0.00864433964108412,5.82148394867342E-13));
#13405=CARTESIAN_POINT('',(0.000258602011535596,-0.00798632071796863,0.00330804455023986));
#13406=CARTESIAN_POINT('',(0.000258602011519632,-0.00611248785617209,0.00611246930479825));
#13407=CARTESIAN_POINT('',(0.000258602011495739,-0.00330797564931162,0.00798632601769886));
#13408=CARTESIAN_POINT('',(0.000258602011476953,-0.00110282992265868,0.00842499999993675));
#13409=CARTESIAN_POINT('',(0.000258602011467558,-1.72799521891854E-12,0.00842500000016943));
#13410=CARTESIAN_POINT('',(0.000258602136233782,-1.72799408318983E-12,0.00842500000008472));
#13411=CARTESIAN_POINT('',(0.000258602131639668,-2.26363092258843E-17,0.00842500002362359));
#13412=CARTESIAN_POINT('',(0.000724069186718163,4.30004688906155E-15,0.00851584589136776));
#13413=CARTESIAN_POINT('',(0.00153614696900967,8.86942973976054E-15,0.00923383480668362));
#13414=CARTESIAN_POINT('',(0.00132239699826857,3.44075559505266E-15,0.0102965150770454));
#13415=CARTESIAN_POINT('',(0.00100623075658947,1.92149073831785E-17,0.0106499998131686));
#13416=CARTESIAN_POINT('',(1.1543600703228E-13,-4.73427093034189E-14,5.83742937136908E-20));
#13417=CARTESIAN_POINT('',(0.00025860201146756,-4.95458259515107E-14,5.44685981140106E-20));
#13418=CARTESIAN_POINT('',(-0.0045,-5.3776427755281E-19,1.47451495458029E-19));
#13419=CARTESIAN_POINT('',(-0.0045,0.,0.));
#13420=CARTESIAN_POINT('',(-0.0045,0.,-0.011075));
#13421=CARTESIAN_POINT('',(-0.0206375,0.,-9.16300179894287E-52));
#13422=CARTESIAN_POINT('',(0.0045,0.,-1.98752982420284E-18));
#13423=CARTESIAN_POINT('',(0.0045,0.,-0.008425));
#13424=CARTESIAN_POINT('',(-0.0206375,0.,0.));
#13425=CARTESIAN_POINT('',(-0.000258602011,-7.31179117070199E-12,0.011075));
#13426=CARTESIAN_POINT('',(-0.000258602011,-0.00144971411674669,0.0110749999990429));
#13427=CARTESIAN_POINT('',(-0.000258602011,-0.00434846651032143,0.0104983454753055));
#13428=CARTESIAN_POINT('',(-0.000258602011,-0.00803511015158343,0.00803508575991702));
#13429=CARTESIAN_POINT('',(-0.000258602011,-0.0104983385114106,0.00434855707665283));
#13430=CARTESIAN_POINT('',(-0.000258602011,-0.0113633307445454,-1.31030853718747E-12));
#13431=CARTESIAN_POINT('',(-0.000258602011,-0.0104983385104078,-0.00434855707907396));
#13432=CARTESIAN_POINT('',(-0.000258602011,-0.00803511014973037,-0.00803508576177009));
#13433=CARTESIAN_POINT('',(-0.000258602011,-0.0043484665079003,-0.0104983454763083));
#13434=CARTESIAN_POINT('',(-0.000258602011,-0.00144971411419257,-0.0110749999993772));
#13435=CARTESIAN_POINT('',(-0.000258602011,-4.75766926220784E-12,-0.011075));
#13436=CARTESIAN_POINT('',(-0.00025860238623378,-9.94454622315446E-13,-0.0110749999999153));
#13437=CARTESIAN_POINT('',(-0.000258602071199268,-6.4246432521501E-12,0.0110749999882117));
#13438=CARTESIAN_POINT('',(-0.000258602011467561,4.51272795225522E-14,-3.71516306442422E-19));
#13439=CARTESIAN_POINT('',(0.0045,-2.22911966663019E-18,1.73472347597681E-20));
#13440=CARTESIAN_POINT('',(0.00450000000033692,3.48751202232752E-13,1.08129136841049E-19));
#13441=CARTESIAN_POINT('',(0.00450000000033692,6.37547546112859E-19,0.00779999999980785));
#13442=CARTESIAN_POINT('',(0.00450000000036139,-1.95000042881955E-12,-0.00779999999974705));
#13443=CARTESIAN_POINT('',(0.00450000000033692,-3.48751060863252E-13,-4.06296004640648E-19));
#13444=CARTESIAN_POINT('',(-1.1543990834159E-13,-4.73314002437894E-14,3.54060453998605E-19));
#13445=CARTESIAN_POINT('',(-0.0010062306454784,7.00818953022586E-18,-0.00885000006260538));
#13446=CARTESIAN_POINT('',(-0.00132239692205273,3.80617846662212E-15,-0.00920348474991875));
#13447=CARTESIAN_POINT('',(-0.00153614703263649,9.26191304452231E-15,-0.0102661649538024));
#13448=CARTESIAN_POINT('',(-0.000724069398158462,4.2080152504004E-15,-0.0109841539795411));
#13449=CARTESIAN_POINT('',(-0.000258602372466113,5.89741576151065E-17,-0.0110749999293739));
#13450=CARTESIAN_POINT('',(-0.00100623071506661,-7.94670107870803E-13,-0.0088500000003638));
#13451=CARTESIAN_POINT('',(-0.000258602011467561,1.98785142045412E-17,0.0110749999998306));
#13452=CARTESIAN_POINT('',(-0.000724069122077457,4.17825833481557E-15,0.0109841541650723));
#13453=CARTESIAN_POINT('',(-0.00153614703309098,9.25202015462542E-15,0.0102661651868448));
#13454=CARTESIAN_POINT('',(-0.00132239696292048,3.81144573458941E-15,0.0092034847956103));
#13455=CARTESIAN_POINT('',(-0.0010062306454784,1.90012882174815E-17,0.00885000006260538));
#13456=CARTESIAN_POINT('',(-0.00100623071506661,-6.59462196535367E-12,0.0088500000003638));
#13457=CARTESIAN_POINT('',(-0.00100623059013322,-6.59462086751533E-12,0.00885000000072759));
#13458=CARTESIAN_POINT('',(-0.00100623059014309,-0.00115846229739644,0.00884999999986943));
#13459=CARTESIAN_POINT('',(-0.00100623059016283,-0.00347484682895264,0.0083891970618622));
#13460=CARTESIAN_POINT('',(-0.00100623059018793,-0.0064208329443351,0.00642081345110636));
#13461=CARTESIAN_POINT('',(-0.00100623059020469,-0.00838919149809096,0.00347491919774606));
#13462=CARTESIAN_POINT('',(-0.00100623059021058,-0.00908040425267338,-2.97546799044951E-12));
#13463=CARTESIAN_POINT('',(-0.00100623059020469,-0.00838919149581363,-0.00347491920324402));
#13464=CARTESIAN_POINT('',(-0.00100623059018793,-0.00642083294012714,-0.00642081345531434));
#13465=CARTESIAN_POINT('',(-0.00100623059016283,-0.00347484682345468,-0.00838919706413948));
#13466=CARTESIAN_POINT('',(-0.00100623059014309,-0.00115846229159649,-0.00885000000062864));
#13467=CARTESIAN_POINT('',(-0.00100623059013322,-7.94669450589741E-13,-0.00885000000072759));
#13468=CARTESIAN_POINT('',(-1.1544007415132E-13,4.73304495273867E-14,-3.69660968558101E-19));
#13469=CARTESIAN_POINT('',(-0.00100623059013322,3.87578284472844E-14,-3.76880161186426E-19));
#13470=CARTESIAN_POINT('',(0.00420000000011192,-3.50891387635993E-13,-4.14898835309052E-19));
#13471=CARTESIAN_POINT('',(0.00420000000019215,8.38119770267861E-18,0.00749999999960454));
#13472=CARTESIAN_POINT('',(0.00435707963295547,-4.05846340527414E-15,0.00749999999964655));
#13473=CARTESIAN_POINT('',(0.00450000000032556,-1.62862306384024E-15,0.00764292036704453));
#13474=CARTESIAN_POINT('',(0.00450000000033692,-3.54563742746683E-19,0.00779999999980785));
#13475=CARTESIAN_POINT('',(0.00419999987517108,-1.5382740212674E-12,0.00749999999980227));
#13476=CARTESIAN_POINT('',(0.00450000000033692,-1.43886481780106E-17,-0.00779999999980785));
#13477=CARTESIAN_POINT('',(0.00450000000032556,-1.62909625669243E-15,-0.00764292036704453));
#13478=CARTESIAN_POINT('',(0.00435707963295547,-4.04642258766554E-15,-0.00749999999964655));
#13479=CARTESIAN_POINT('',(0.00420000000019215,3.31895800936513E-17,-0.00749999999960454));
#13480=CARTESIAN_POINT('',(0.00419999987509607,-4.29142485976802E-12,-0.00749999999980227));
#13481=CARTESIAN_POINT('',(0.00420000000019215,-4.29142066913366E-12,-0.00749999999960454));
#13482=CARTESIAN_POINT('',(0.00420000000020615,-0.00196349541225418,-0.00749999999857291));
#13483=CARTESIAN_POINT('',(0.00420000000023406,-0.0058748540154159,-0.00587708718402969));
#13484=CARTESIAN_POINT('',(0.00420000000025145,-0.00831257299276455,1.52571835373982E-12));
#13485=CARTESIAN_POINT('',(0.00420000000023406,-0.0058748540132585,0.00587708718618627));
#13486=CARTESIAN_POINT('',(0.00420000000020615,-0.00196349540950103,0.00749999999929369));
#13487=CARTESIAN_POINT('',(0.00420000000019215,-1.53826945716326E-12,0.00749999999960454));
#13488=CARTESIAN_POINT('',(0.00420000000011192,3.50891535870921E-13,1.16083160393565E-19));
#13489=CARTESIAN_POINT('',(0.00420000000011192,3.50891535870921E-13,1.16083160393565E-19));
#13490=CARTESIAN_POINT('',(-0.0206375,0.,0.));
#13491=CARTESIAN_POINT('',(-0.0045,0.,0.));
#13492=CARTESIAN_POINT('',(-0.0045,0.,-0.00885));
#13493=CARTESIAN_POINT('',(-0.0206375,0.,-2.47065262083525E-51));
#13494=CARTESIAN_POINT('',(-0.0042,-3.22189792023104E-12,-0.0075));
#13495=CARTESIAN_POINT('',(-0.0042,-0.0019634954110344,-0.00749999999915651));
#13496=CARTESIAN_POINT('',(-0.0042,-0.00587485401406066,-0.00587708718534322));
#13497=CARTESIAN_POINT('',(-0.0042,-0.00831257299263083,-9.5852737806285E-13));
#13498=CARTESIAN_POINT('',(-0.0042,-0.00587485401541604,0.00587708718398836));
#13499=CARTESIAN_POINT('',(-0.0042,-0.00196349541276405,0.00749999999870368));
#13500=CARTESIAN_POINT('',(-0.0042,-4.95155158286816E-12,0.0075));
#13501=CARTESIAN_POINT('',(-0.00419999962509607,-1.53827397134479E-12,0.00749999999980227));
#13502=CARTESIAN_POINT('',(-0.00420000000009607,-3.48594912388589E-12,-0.00749999999980227));
#13503=CARTESIAN_POINT('',(-0.00420000000011191,3.50891751372691E-13,2.79083595183788E-19));
#13504=CARTESIAN_POINT('',(-0.0045,-4.07660016854549E-19,-7.28583859910259E-19));
#13505=CARTESIAN_POINT('',(-0.00450000000033692,3.48751417212871E-13,2.87745340681233E-19));
#13506=CARTESIAN_POINT('',(-0.00450000000033692,-2.42388042693057E-19,-0.00779999999980785));
#13507=CARTESIAN_POINT('',(-0.00450000000036139,-1.9500002825196E-12,0.00779999999974705));
#13508=CARTESIAN_POINT('',(-0.00450000000033692,-3.48750946764454E-13,-1.41700427235676E-19));
#13509=CARTESIAN_POINT('',(-0.00420000000011191,-3.50891287789699E-13,-1.29656749332468E-19));
#13510=CARTESIAN_POINT('',(-0.00450000000033692,-2.40464944123498E-19,0.00779999999980786));
#13511=CARTESIAN_POINT('',(-0.00450000000032556,-1.62850896504167E-15,0.00764292036704453));
#13512=CARTESIAN_POINT('',(-0.00435707963295547,-4.05835609638575E-15,0.00749999999964656));
#13513=CARTESIAN_POINT('',(-0.00420000000019214,8.48104399744249E-18,0.00749999999960455));
#13514=CARTESIAN_POINT('',(-0.00420000000019214,3.32894263884152E-17,-0.00749999999960455));
#13515=CARTESIAN_POINT('',(-0.00435707963295547,-4.04631527877715E-15,-0.00749999999964656));
#13516=CARTESIAN_POINT('',(-0.00450000000032556,-1.62898215789386E-15,-0.00764292036704453));
#13517=CARTESIAN_POINT('',(-0.00450000000033692,-1.42745493793874E-17,-0.00779999999980786));
#13518=CARTESIAN_POINT('',(-0.00420000000011191,3.50891751372691E-13,2.79083595183788E-19));
#18809=MECHANICAL_DESIGN_GEOMETRIC_PRESENTATION_REPRESENTATION('',(#8177),#18810);
#18810=(
GEOMETRIC_REPRESENTATION_CONTEXT(3)
GLOBAL_UNCERTAINTY_ASSIGNED_CONTEXT((#18817))
GLOBAL_UNIT_ASSIGNED_CONTEXT((#18826,#18825,#18824))
REPRESENTATION_CONTEXT('MAS-697','TOP_LEVEL_ASSEMBLY_PART')
);
#18814=(
GEOMETRIC_REPRESENTATION_CONTEXT(3)
GLOBAL_UNCERTAINTY_ASSIGNED_CONTEXT((#18821))
GLOBAL_UNIT_ASSIGNED_CONTEXT((#18826,#18825,#18824))
REPRESENTATION_CONTEXT(
'angular contact ball bearing_68_bsi_BS 6267 ABB - 4815 - 18,SI,NC,18_
68__ DE    23193','COMPONENT_PART')
);
#18817=UNCERTAINTY_MEASURE_WITH_UNIT(LENGTH_MEASURE(1.E-8),#18826,
'DISTANCE_ACCURACY_VALUE','Maximum Tolerance applied to model');
#18821=UNCERTAINTY_MEASURE_WITH_UNIT(LENGTH_MEASURE(2.E-5),#18826,
'DISTANCE_ACCURACY_VALUE','Maximum Tolerance applied to model');
#18824=(
NAMED_UNIT(*)
SI_UNIT($,.STERADIAN.)
SOLID_ANGLE_UNIT()
);
#18825=(
NAMED_UNIT(*)
PLANE_ANGLE_UNIT()
SI_UNIT($,.RADIAN.)
);
#18826=(
LENGTH_UNIT()
NAMED_UNIT(*)
SI_UNIT($,.METRE.)
);
#18834=PRODUCT_DEFINITION_SHAPE('','',#18844);
#18844=PRODUCT_DEFINITION('','',#18858,#18851);
#18851=PRODUCT_DEFINITION_CONTEXT('',#18890,'design');
#18858=PRODUCT_DEFINITION_FORMATION_WITH_SPECIFIED_SOURCE('','',#18872,
 .NOT_KNOWN.);
#18872=PRODUCT(
'angular contact ball bearing_68_bsi_BS 6267 ABB - 4815 - 18,SI,NC,18_
68__ DE    23193',
'angular contact ball bearing_68_bsi_BS 6267 ABB - 4815 - 18,SI,NC,18_
68__ DE    23193',
'angular contact ball bearing_68_bsi_BS 6267 ABB - 4815 - 18,SI,NC,18_
68__ DE    23193',(#18886));
#18886=PRODUCT_CONTEXT('',#18890,'mechanical');
#18890=APPLICATION_CONTEXT('managed model based 3d engineering');
ENDSEC;
END-ISO-10303-21;
